ISO-10303-21;
HEADER;
/* Generated by software containing ST-Developer
 * from STEP Tools, Inc. (www.steptools.com) 
 */

FILE_DESCRIPTION(
/* description */ (''),
/* implementation_level */ '2;1');

FILE_NAME(
/* name */ 'Front_Block_01.step',
/* time_stamp */ '2026-10-23T22:30:33+06:00',
/* author */ (''),
/* organization */ (''),
/* preprocessor_version */ 'ST-DEVELOPER v20.2',
/* originating_system */ 'Autodesk Translation Framework v15.15.0.0',
/* authorisation */ '');

FILE_SCHEMA (('AUTOMOTIVE_DESIGN { 1 0 10303 214 3 1 1 }'));
ENDSEC;

DATA;
#10=MECHANICAL_DESIGN_GEOMETRIC_PRESENTATION_REPRESENTATION('',(#241),#10131);
#115=ELLIPSE('',#6340,2.82842712474619,2.);
#116=ELLIPSE('',#6341,2.82842712474619,2.);
#117=ELLIPSE('',#6343,2.8284271247462,2.);
#118=ELLIPSE('',#6345,2.8284271247462,2.);
#119=ELLIPSE('',#6357,1.08239220029239,1.);
#120=ELLIPSE('',#6359,1.0823922002924,1.);
#121=ELLIPSE('',#6362,1.0823922002924,1.);
#122=ELLIPSE('',#6364,1.0823922002924,1.);
#123=ELLIPSE('',#6365,1.0823922002924,1.);
#124=ELLIPSE('',#6367,1.08239220029239,1.);
#125=ELLIPSE('',#6369,1.0823922002924,1.);
#126=ELLIPSE('',#6371,1.08239220029239,1.);
#127=ELLIPSE('',#6373,1.0823922002924,1.);
#128=ELLIPSE('',#6381,1.0823922002924,1.);
#129=ELLIPSE('',#6382,1.08239220029239,1.);
#130=ELLIPSE('',#6384,1.08239220029239,1.);
#131=ELLIPSE('',#6386,1.08239220029239,1.);
#132=ELLIPSE('',#6388,1.08239220029239,1.);
#133=ELLIPSE('',#6390,1.0823922002924,1.);
#134=ELLIPSE('',#6392,1.08239220029239,1.);
#221=SHAPE_REPRESENTATION_RELATIONSHIP('SRR','None',#10175,#231);
#231=ADVANCED_BREP_SHAPE_REPRESENTATION('',(#251),#10127);
#241=STYLED_ITEM('',(#10247),#251);
#251=MANIFOLD_SOLID_BREP('Front_Block_01',#5885);
#305=FACE_BOUND('',#1064,.T.);
#306=FACE_BOUND('',#1065,.T.);
#307=FACE_BOUND('',#1066,.T.);
#408=PLANE('',#6330);
#409=PLANE('',#6334);
#410=PLANE('',#6338);
#411=PLANE('',#6347);
#412=PLANE('',#6350);
#413=PLANE('',#6351);
#414=PLANE('',#6352);
#415=PLANE('',#6355);
#416=PLANE('',#6360);
#417=PLANE('',#6376);
#418=PLANE('',#6377);
#419=PLANE('',#6378);
#420=PLANE('',#6379);
#421=PLANE('',#6395);
#422=PLANE('',#6396);
#423=PLANE('',#6397);
#424=PLANE('',#6398);
#652=FACE_OUTER_BOUND('',#1051,.T.);
#653=FACE_OUTER_BOUND('',#1052,.T.);
#654=FACE_OUTER_BOUND('',#1053,.T.);
#655=FACE_OUTER_BOUND('',#1054,.T.);
#656=FACE_OUTER_BOUND('',#1055,.T.);
#657=FACE_OUTER_BOUND('',#1056,.T.);
#658=FACE_OUTER_BOUND('',#1057,.T.);
#659=FACE_OUTER_BOUND('',#1058,.T.);
#660=FACE_OUTER_BOUND('',#1059,.T.);
#661=FACE_OUTER_BOUND('',#1060,.T.);
#662=FACE_OUTER_BOUND('',#1061,.T.);
#663=FACE_OUTER_BOUND('',#1062,.T.);
#664=FACE_OUTER_BOUND('',#1063,.T.);
#665=FACE_OUTER_BOUND('',#1067,.T.);
#666=FACE_OUTER_BOUND('',#1068,.T.);
#667=FACE_OUTER_BOUND('',#1069,.T.);
#668=FACE_OUTER_BOUND('',#1070,.T.);
#669=FACE_OUTER_BOUND('',#1071,.T.);
#670=FACE_OUTER_BOUND('',#1072,.T.);
#671=FACE_OUTER_BOUND('',#1073,.T.);
#672=FACE_OUTER_BOUND('',#1074,.T.);
#673=FACE_OUTER_BOUND('',#1075,.T.);
#674=FACE_OUTER_BOUND('',#1076,.T.);
#675=FACE_OUTER_BOUND('',#1077,.T.);
#676=FACE_OUTER_BOUND('',#1078,.T.);
#677=FACE_OUTER_BOUND('',#1079,.T.);
#678=FACE_OUTER_BOUND('',#1080,.T.);
#679=FACE_OUTER_BOUND('',#1081,.T.);
#680=FACE_OUTER_BOUND('',#1082,.T.);
#681=FACE_OUTER_BOUND('',#1083,.T.);
#682=FACE_OUTER_BOUND('',#1084,.T.);
#683=FACE_OUTER_BOUND('',#1085,.T.);
#684=FACE_OUTER_BOUND('',#1086,.T.);
#685=FACE_OUTER_BOUND('',#1087,.T.);
#686=FACE_OUTER_BOUND('',#1088,.T.);
#687=FACE_OUTER_BOUND('',#1089,.T.);
#688=FACE_OUTER_BOUND('',#1090,.T.);
#689=FACE_OUTER_BOUND('',#1091,.T.);
#690=FACE_OUTER_BOUND('',#1092,.T.);
#691=FACE_OUTER_BOUND('',#1093,.T.);
#692=FACE_OUTER_BOUND('',#1094,.T.);
#693=FACE_OUTER_BOUND('',#1095,.T.);
#1051=EDGE_LOOP('',(#4594,#4595,#4596,#4597));
#1052=EDGE_LOOP('',(#4598));
#1053=EDGE_LOOP('',(#4599,#4600,#4601,#4602));
#1054=EDGE_LOOP('',(#4603));
#1055=EDGE_LOOP('',(#4604,#4605,#4606,#4607));
#1056=EDGE_LOOP('',(#4608));
#1057=EDGE_LOOP('',(#4609,#4610,#4611,#4612));
#1058=EDGE_LOOP('',(#4613,#4614,#4615,#4616));
#1059=EDGE_LOOP('',(#4617,#4618,#4619,#4620));
#1060=EDGE_LOOP('',(#4621,#4622,#4623,#4624));
#1061=EDGE_LOOP('',(#4625,#4626,#4627,#4628,#4629,#4630));
#1062=EDGE_LOOP('',(#4631,#4632,#4633,#4634,#4635,#4636,#4637,#4638,#4639,
#4640,#4641,#4642));
#1063=EDGE_LOOP('',(#4643,#4644,#4645,#4646));
#1064=EDGE_LOOP('',(#4647));
#1065=EDGE_LOOP('',(#4648));
#1066=EDGE_LOOP('',(#4649));
#1067=EDGE_LOOP('',(#4650,#4651,#4652,#4653,#4654,#4655));
#1068=EDGE_LOOP('',(#4656,#4657,#4658,#4659,#4660,#4661,#4662,#4663,#4664,
#4665,#4666,#4667));
#1069=EDGE_LOOP('',(#4668,#4669,#4670,#4671));
#1070=EDGE_LOOP('',(#4672,#4673,#4674,#4675));
#1071=EDGE_LOOP('',(#4676,#4677,#4678,#4679));
#1072=EDGE_LOOP('',(#4680,#4681,#4682,#4683));
#1073=EDGE_LOOP('',(#4684,#4685,#4686,#4687));
#1074=EDGE_LOOP('',(#4688,#4689,#4690,#4691));
#1075=EDGE_LOOP('',(#4692,#4693,#4694,#4695));
#1076=EDGE_LOOP('',(#4696,#4697,#4698,#4699));
#1077=EDGE_LOOP('',(#4700,#4701,#4702,#4703));
#1078=EDGE_LOOP('',(#4704,#4705,#4706,#4707));
#1079=EDGE_LOOP('',(#4708,#4709,#4710,#4711));
#1080=EDGE_LOOP('',(#4712,#4713,#4714,#4715));
#1081=EDGE_LOOP('',(#4716,#4717,#4718,#4719));
#1082=EDGE_LOOP('',(#4720,#4721,#4722,#4723));
#1083=EDGE_LOOP('',(#4724,#4725,#4726,#4727));
#1084=EDGE_LOOP('',(#4728,#4729,#4730,#4731));
#1085=EDGE_LOOP('',(#4732,#4733,#4734,#4735));
#1086=EDGE_LOOP('',(#4736,#4737,#4738,#4739));
#1087=EDGE_LOOP('',(#4740,#4741,#4742,#4743));
#1088=EDGE_LOOP('',(#4744,#4745,#4746,#4747));
#1089=EDGE_LOOP('',(#4748,#4749,#4750,#4751));
#1090=EDGE_LOOP('',(#4752,#4753,#4754,#4755));
#1091=EDGE_LOOP('',(#4756,#4757,#4758,#4759));
#1092=EDGE_LOOP('',(#4760,#4761,#4762,#4763));
#1093=EDGE_LOOP('',(#4764,#4765,#4766,#4767));
#1094=EDGE_LOOP('',(#4768,#4769,#4770,#4771));
#1095=EDGE_LOOP('',(#4772,#4773,#4774,#4775));
#1535=LINE('',#9354,#2085);
#1536=LINE('',#9361,#2086);
#1537=LINE('',#9368,#2087);
#1538=LINE('',#9374,#2088);
#1539=LINE('',#9378,#2089);
#1540=LINE('',#9382,#2090);
#1541=LINE('',#9384,#2091);
#1542=LINE('',#9388,#2092);
#1543=LINE('',#9390,#2093);
#1544=LINE('',#9393,#2094);
#1545=LINE('',#9394,#2095);
#1546=LINE('',#9397,#2096);
#1547=LINE('',#9401,#2097);
#1548=LINE('',#9404,#2098);
#1549=LINE('',#9407,#2099);
#1550=LINE('',#9409,#2100);
#1551=LINE('',#9411,#2101);
#1552=LINE('',#9413,#2102);
#1553=LINE('',#9415,#2103);
#1554=LINE('',#9417,#2104);
#1555=LINE('',#9419,#2105);
#1556=LINE('',#9421,#2106);
#1557=LINE('',#9423,#2107);
#1558=LINE('',#9424,#2108);
#1559=LINE('',#9428,#2109);
#1560=LINE('',#9432,#2110);
#1561=LINE('',#9436,#2111);
#1562=LINE('',#9438,#2112);
#1563=LINE('',#9440,#2113);
#1564=LINE('',#9442,#2114);
#1565=LINE('',#9444,#2115);
#1566=LINE('',#9446,#2116);
#1567=LINE('',#9448,#2117);
#1568=LINE('',#9450,#2118);
#1569=LINE('',#9451,#2119);
#1570=LINE('',#9454,#2120);
#1571=LINE('',#9459,#2121);
#1572=LINE('',#9462,#2122);
#1573=LINE('',#9463,#2123);
#1574=LINE('',#9469,#2124);
#1575=LINE('',#9474,#2125);
#1576=LINE('',#9478,#2126);
#1577=LINE('',#9482,#2127);
#1578=LINE('',#9486,#2128);
#1579=LINE('',#9489,#2129);
#1580=LINE('',#9491,#2130);
#1581=LINE('',#9494,#2131);
#1582=LINE('',#9496,#2132);
#1583=LINE('',#9497,#2133);
#1584=LINE('',#9500,#2134);
#1585=LINE('',#9501,#2135);
#1586=LINE('',#9504,#2136);
#1587=LINE('',#9505,#2137);
#1588=LINE('',#9508,#2138);
#1589=LINE('',#9509,#2139);
#1590=LINE('',#9521,#2140);
#1591=LINE('',#9525,#2141);
#1592=LINE('',#9528,#2142);
#1593=LINE('',#9530,#2143);
#1594=LINE('',#9532,#2144);
#1595=LINE('',#9533,#2145);
#2085=VECTOR('',#7581,3.);
#2086=VECTOR('',#7590,3.);
#2087=VECTOR('',#7599,3.);
#2088=VECTOR('',#7606,10.);
#2089=VECTOR('',#7609,10.);
#2090=VECTOR('',#7614,10.);
#2091=VECTOR('',#7615,10.);
#2092=VECTOR('',#7620,10.);
#2093=VECTOR('',#7621,10.);
#2094=VECTOR('',#7626,10.);
#2095=VECTOR('',#7627,10.);
#2096=VECTOR('',#7630,10.);
#2097=VECTOR('',#7633,10.);
#2098=VECTOR('',#7636,10.);
#2099=VECTOR('',#7639,10.);
#2100=VECTOR('',#7640,10.);
#2101=VECTOR('',#7641,10.);
#2102=VECTOR('',#7642,10.);
#2103=VECTOR('',#7643,10.);
#2104=VECTOR('',#7644,10.);
#2105=VECTOR('',#7645,10.);
#2106=VECTOR('',#7646,10.);
#2107=VECTOR('',#7647,10.);
#2108=VECTOR('',#7648,10.);
#2109=VECTOR('',#7653,10.);
#2110=VECTOR('',#7656,10.);
#2111=VECTOR('',#7661,10.);
#2112=VECTOR('',#7662,10.);
#2113=VECTOR('',#7663,10.);
#2114=VECTOR('',#7664,10.);
#2115=VECTOR('',#7665,10.);
#2116=VECTOR('',#7666,10.);
#2117=VECTOR('',#7667,10.);
#2118=VECTOR('',#7668,10.);
#2119=VECTOR('',#7669,10.);
#2120=VECTOR('',#7672,10.);
#2121=VECTOR('',#7679,10.);
#2122=VECTOR('',#7682,10.);
#2123=VECTOR('',#7683,10.);
#2124=VECTOR('',#7690,10.);
#2125=VECTOR('',#7697,10.);
#2126=VECTOR('',#7702,10.);
#2127=VECTOR('',#7707,10.);
#2128=VECTOR('',#7712,10.);
#2129=VECTOR('',#7717,10.);
#2130=VECTOR('',#7720,10.);
#2131=VECTOR('',#7723,10.);
#2132=VECTOR('',#7724,10.);
#2133=VECTOR('',#7725,10.);
#2134=VECTOR('',#7728,10.);
#2135=VECTOR('',#7729,10.);
#2136=VECTOR('',#7732,10.);
#2137=VECTOR('',#7733,10.);
#2138=VECTOR('',#7736,10.);
#2139=VECTOR('',#7737,10.);
#2140=VECTOR('',#7758,10.);
#2141=VECTOR('',#7763,10.);
#2142=VECTOR('',#7768,10.);
#2143=VECTOR('',#7771,10.);
#2144=VECTOR('',#7774,10.);
#2145=VECTOR('',#7775,10.);
#2404=CIRCLE('',#6328,3.);
#2405=CIRCLE('',#6329,3.);
#2406=CIRCLE('',#6332,3.);
#2407=CIRCLE('',#6333,3.);
#2408=CIRCLE('',#6336,3.);
#2409=CIRCLE('',#6337,3.);
#2410=CIRCLE('',#6348,1.);
#2411=CIRCLE('',#6349,1.);
#2412=CIRCLE('',#6353,1.);
#2413=CIRCLE('',#6354,1.);
#2696=VERTEX_POINT('',#9351);
#2697=VERTEX_POINT('',#9353);
#2698=VERTEX_POINT('',#9358);
#2699=VERTEX_POINT('',#9360);
#2700=VERTEX_POINT('',#9365);
#2701=VERTEX_POINT('',#9367);
#2702=VERTEX_POINT('',#9372);
#2703=VERTEX_POINT('',#9373);
#2704=VERTEX_POINT('',#9375);
#2705=VERTEX_POINT('',#9377);
#2706=VERTEX_POINT('',#9381);
#2707=VERTEX_POINT('',#9383);
#2708=VERTEX_POINT('',#9387);
#2709=VERTEX_POINT('',#9389);
#2710=VERTEX_POINT('',#9396);
#2711=VERTEX_POINT('',#9398);
#2712=VERTEX_POINT('',#9400);
#2713=VERTEX_POINT('',#9402);
#2714=VERTEX_POINT('',#9406);
#2715=VERTEX_POINT('',#9408);
#2716=VERTEX_POINT('',#9410);
#2717=VERTEX_POINT('',#9412);
#2718=VERTEX_POINT('',#9414);
#2719=VERTEX_POINT('',#9416);
#2720=VERTEX_POINT('',#9418);
#2721=VERTEX_POINT('',#9420);
#2722=VERTEX_POINT('',#9422);
#2723=VERTEX_POINT('',#9427);
#2724=VERTEX_POINT('',#9429);
#2725=VERTEX_POINT('',#9431);
#2726=VERTEX_POINT('',#9435);
#2727=VERTEX_POINT('',#9437);
#2728=VERTEX_POINT('',#9439);
#2729=VERTEX_POINT('',#9441);
#2730=VERTEX_POINT('',#9443);
#2731=VERTEX_POINT('',#9445);
#2732=VERTEX_POINT('',#9447);
#2733=VERTEX_POINT('',#9449);
#2734=VERTEX_POINT('',#9453);
#2735=VERTEX_POINT('',#9457);
#2736=VERTEX_POINT('',#9461);
#2737=VERTEX_POINT('',#9467);
#2738=VERTEX_POINT('',#9468);
#2739=VERTEX_POINT('',#9473);
#2740=VERTEX_POINT('',#9477);
#2741=VERTEX_POINT('',#9481);
#2742=VERTEX_POINT('',#9485);
#2743=VERTEX_POINT('',#9493);
#2744=VERTEX_POINT('',#9495);
#2745=VERTEX_POINT('',#9499);
#2746=VERTEX_POINT('',#9503);
#2747=VERTEX_POINT('',#9507);
#2748=VERTEX_POINT('',#9520);
#2749=VERTEX_POINT('',#9524);
#3349=EDGE_CURVE('',#2696,#2696,#2404,.T.);
#3350=EDGE_CURVE('',#2696,#2697,#1535,.T.);
#3351=EDGE_CURVE('',#2697,#2697,#2405,.T.);
#3352=EDGE_CURVE('',#2698,#2698,#2406,.T.);
#3353=EDGE_CURVE('',#2698,#2699,#1536,.T.);
#3354=EDGE_CURVE('',#2699,#2699,#2407,.T.);
#3355=EDGE_CURVE('',#2700,#2700,#2408,.T.);
#3356=EDGE_CURVE('',#2700,#2701,#1537,.T.);
#3357=EDGE_CURVE('',#2701,#2701,#2409,.T.);
#3358=EDGE_CURVE('',#2702,#2703,#1538,.T.);
#3359=EDGE_CURVE('',#2703,#2704,#115,.T.);
#3360=EDGE_CURVE('',#2704,#2705,#1539,.T.);
#3361=EDGE_CURVE('',#2705,#2702,#116,.T.);
#3362=EDGE_CURVE('',#2706,#2704,#1540,.T.);
#3363=EDGE_CURVE('',#2703,#2707,#1541,.T.);
#3364=EDGE_CURVE('',#2707,#2706,#117,.T.);
#3365=EDGE_CURVE('',#2708,#2702,#1542,.T.);
#3366=EDGE_CURVE('',#2705,#2709,#1543,.T.);
#3367=EDGE_CURVE('',#2709,#2708,#118,.T.);
#3368=EDGE_CURVE('',#2709,#2706,#1544,.T.);
#3369=EDGE_CURVE('',#2707,#2708,#1545,.T.);
#3370=EDGE_CURVE('',#2705,#2710,#1546,.T.);
#3371=EDGE_CURVE('',#2711,#2710,#2410,.T.);
#3372=EDGE_CURVE('',#2712,#2711,#1547,.T.);
#3373=EDGE_CURVE('',#2713,#2712,#2411,.T.);
#3374=EDGE_CURVE('',#2709,#2713,#1548,.T.);
#3375=EDGE_CURVE('',#2714,#2704,#1549,.T.);
#3376=EDGE_CURVE('',#2715,#2714,#1550,.T.);
#3377=EDGE_CURVE('',#2716,#2715,#1551,.T.);
#3378=EDGE_CURVE('',#2717,#2716,#1552,.T.);
#3379=EDGE_CURVE('',#2718,#2717,#1553,.T.);
#3380=EDGE_CURVE('',#2719,#2718,#1554,.T.);
#3381=EDGE_CURVE('',#2720,#2719,#1555,.T.);
#3382=EDGE_CURVE('',#2721,#2720,#1556,.T.);
#3383=EDGE_CURVE('',#2722,#2721,#1557,.T.);
#3384=EDGE_CURVE('',#2710,#2722,#1558,.T.);
#3385=EDGE_CURVE('',#2723,#2706,#1559,.T.);
#3386=EDGE_CURVE('',#2724,#2723,#2412,.T.);
#3387=EDGE_CURVE('',#2725,#2724,#1560,.T.);
#3388=EDGE_CURVE('',#2714,#2725,#2413,.T.);
#3389=EDGE_CURVE('',#2726,#2713,#1561,.T.);
#3390=EDGE_CURVE('',#2727,#2726,#1562,.T.);
#3391=EDGE_CURVE('',#2728,#2727,#1563,.T.);
#3392=EDGE_CURVE('',#2729,#2728,#1564,.T.);
#3393=EDGE_CURVE('',#2730,#2729,#1565,.T.);
#3394=EDGE_CURVE('',#2731,#2730,#1566,.T.);
#3395=EDGE_CURVE('',#2732,#2731,#1567,.T.);
#3396=EDGE_CURVE('',#2733,#2732,#1568,.T.);
#3397=EDGE_CURVE('',#2723,#2733,#1569,.T.);
#3398=EDGE_CURVE('',#2712,#2734,#1570,.T.);
#3399=EDGE_CURVE('',#2734,#2726,#119,.T.);
#3400=EDGE_CURVE('',#2735,#2733,#120,.T.);
#3401=EDGE_CURVE('',#2735,#2724,#1571,.T.);
#3402=EDGE_CURVE('',#2736,#2711,#1572,.T.);
#3403=EDGE_CURVE('',#2734,#2736,#1573,.T.);
#3404=EDGE_CURVE('',#2722,#2736,#121,.T.);
#3405=EDGE_CURVE('',#2737,#2738,#1574,.T.);
#3406=EDGE_CURVE('',#2738,#2728,#122,.T.);
#3407=EDGE_CURVE('',#2727,#2737,#123,.T.);
#3408=EDGE_CURVE('',#2738,#2739,#1575,.T.);
#3409=EDGE_CURVE('',#2739,#2729,#124,.T.);
#3410=EDGE_CURVE('',#2739,#2740,#1576,.T.);
#3411=EDGE_CURVE('',#2740,#2730,#125,.T.);
#3412=EDGE_CURVE('',#2740,#2741,#1577,.T.);
#3413=EDGE_CURVE('',#2741,#2731,#126,.T.);
#3414=EDGE_CURVE('',#2741,#2742,#1578,.T.);
#3415=EDGE_CURVE('',#2742,#2732,#127,.T.);
#3416=EDGE_CURVE('',#2742,#2735,#1579,.T.);
#3417=EDGE_CURVE('',#2734,#2737,#1580,.T.);
#3418=EDGE_CURVE('',#2740,#2743,#1581,.T.);
#3419=EDGE_CURVE('',#2744,#2743,#1582,.T.);
#3420=EDGE_CURVE('',#2744,#2741,#1583,.T.);
#3421=EDGE_CURVE('',#2745,#2739,#1584,.T.);
#3422=EDGE_CURVE('',#2743,#2745,#1585,.T.);
#3423=EDGE_CURVE('',#2738,#2746,#1586,.T.);
#3424=EDGE_CURVE('',#2745,#2746,#1587,.T.);
#3425=EDGE_CURVE('',#2747,#2737,#1588,.T.);
#3426=EDGE_CURVE('',#2746,#2747,#1589,.T.);
#3427=EDGE_CURVE('',#2720,#2746,#128,.T.);
#3428=EDGE_CURVE('',#2721,#2747,#129,.T.);
#3429=EDGE_CURVE('',#2719,#2745,#130,.T.);
#3430=EDGE_CURVE('',#2718,#2743,#131,.T.);
#3431=EDGE_CURVE('',#2717,#2744,#132,.T.);
#3432=EDGE_CURVE('',#2748,#2744,#1590,.T.);
#3433=EDGE_CURVE('',#2716,#2748,#133,.T.);
#3434=EDGE_CURVE('',#2749,#2748,#1591,.T.);
#3435=EDGE_CURVE('',#2715,#2749,#134,.T.);
#3436=EDGE_CURVE('',#2725,#2749,#1592,.T.);
#3437=EDGE_CURVE('',#2747,#2736,#1593,.T.);
#3438=EDGE_CURVE('',#2742,#2748,#1594,.T.);
#3439=EDGE_CURVE('',#2749,#2735,#1595,.T.);
#4594=ORIENTED_EDGE('',*,*,#3349,.F.);
#4595=ORIENTED_EDGE('',*,*,#3350,.T.);
#4596=ORIENTED_EDGE('',*,*,#3351,.T.);
#4597=ORIENTED_EDGE('',*,*,#3350,.F.);
#4598=ORIENTED_EDGE('',*,*,#3351,.F.);
#4599=ORIENTED_EDGE('',*,*,#3352,.F.);
#4600=ORIENTED_EDGE('',*,*,#3353,.T.);
#4601=ORIENTED_EDGE('',*,*,#3354,.T.);
#4602=ORIENTED_EDGE('',*,*,#3353,.F.);
#4603=ORIENTED_EDGE('',*,*,#3354,.F.);
#4604=ORIENTED_EDGE('',*,*,#3355,.F.);
#4605=ORIENTED_EDGE('',*,*,#3356,.T.);
#4606=ORIENTED_EDGE('',*,*,#3357,.T.);
#4607=ORIENTED_EDGE('',*,*,#3356,.F.);
#4608=ORIENTED_EDGE('',*,*,#3357,.F.);
#4609=ORIENTED_EDGE('',*,*,#3358,.T.);
#4610=ORIENTED_EDGE('',*,*,#3359,.T.);
#4611=ORIENTED_EDGE('',*,*,#3360,.T.);
#4612=ORIENTED_EDGE('',*,*,#3361,.T.);
#4613=ORIENTED_EDGE('',*,*,#3362,.T.);
#4614=ORIENTED_EDGE('',*,*,#3359,.F.);
#4615=ORIENTED_EDGE('',*,*,#3363,.T.);
#4616=ORIENTED_EDGE('',*,*,#3364,.T.);
#4617=ORIENTED_EDGE('',*,*,#3365,.T.);
#4618=ORIENTED_EDGE('',*,*,#3361,.F.);
#4619=ORIENTED_EDGE('',*,*,#3366,.T.);
#4620=ORIENTED_EDGE('',*,*,#3367,.T.);
#4621=ORIENTED_EDGE('',*,*,#3368,.T.);
#4622=ORIENTED_EDGE('',*,*,#3364,.F.);
#4623=ORIENTED_EDGE('',*,*,#3369,.T.);
#4624=ORIENTED_EDGE('',*,*,#3367,.F.);
#4625=ORIENTED_EDGE('',*,*,#3366,.F.);
#4626=ORIENTED_EDGE('',*,*,#3370,.T.);
#4627=ORIENTED_EDGE('',*,*,#3371,.F.);
#4628=ORIENTED_EDGE('',*,*,#3372,.F.);
#4629=ORIENTED_EDGE('',*,*,#3373,.F.);
#4630=ORIENTED_EDGE('',*,*,#3374,.F.);
#4631=ORIENTED_EDGE('',*,*,#3360,.F.);
#4632=ORIENTED_EDGE('',*,*,#3375,.F.);
#4633=ORIENTED_EDGE('',*,*,#3376,.F.);
#4634=ORIENTED_EDGE('',*,*,#3377,.F.);
#4635=ORIENTED_EDGE('',*,*,#3378,.F.);
#4636=ORIENTED_EDGE('',*,*,#3379,.F.);
#4637=ORIENTED_EDGE('',*,*,#3380,.F.);
#4638=ORIENTED_EDGE('',*,*,#3381,.F.);
#4639=ORIENTED_EDGE('',*,*,#3382,.F.);
#4640=ORIENTED_EDGE('',*,*,#3383,.F.);
#4641=ORIENTED_EDGE('',*,*,#3384,.F.);
#4642=ORIENTED_EDGE('',*,*,#3370,.F.);
#4643=ORIENTED_EDGE('',*,*,#3358,.F.);
#4644=ORIENTED_EDGE('',*,*,#3365,.F.);
#4645=ORIENTED_EDGE('',*,*,#3369,.F.);
#4646=ORIENTED_EDGE('',*,*,#3363,.F.);
#4647=ORIENTED_EDGE('',*,*,#3349,.T.);
#4648=ORIENTED_EDGE('',*,*,#3352,.T.);
#4649=ORIENTED_EDGE('',*,*,#3355,.T.);
#4650=ORIENTED_EDGE('',*,*,#3362,.F.);
#4651=ORIENTED_EDGE('',*,*,#3385,.F.);
#4652=ORIENTED_EDGE('',*,*,#3386,.F.);
#4653=ORIENTED_EDGE('',*,*,#3387,.F.);
#4654=ORIENTED_EDGE('',*,*,#3388,.F.);
#4655=ORIENTED_EDGE('',*,*,#3375,.T.);
#4656=ORIENTED_EDGE('',*,*,#3368,.F.);
#4657=ORIENTED_EDGE('',*,*,#3374,.T.);
#4658=ORIENTED_EDGE('',*,*,#3389,.F.);
#4659=ORIENTED_EDGE('',*,*,#3390,.F.);
#4660=ORIENTED_EDGE('',*,*,#3391,.F.);
#4661=ORIENTED_EDGE('',*,*,#3392,.F.);
#4662=ORIENTED_EDGE('',*,*,#3393,.F.);
#4663=ORIENTED_EDGE('',*,*,#3394,.F.);
#4664=ORIENTED_EDGE('',*,*,#3395,.F.);
#4665=ORIENTED_EDGE('',*,*,#3396,.F.);
#4666=ORIENTED_EDGE('',*,*,#3397,.F.);
#4667=ORIENTED_EDGE('',*,*,#3385,.T.);
#4668=ORIENTED_EDGE('',*,*,#3373,.T.);
#4669=ORIENTED_EDGE('',*,*,#3398,.T.);
#4670=ORIENTED_EDGE('',*,*,#3399,.T.);
#4671=ORIENTED_EDGE('',*,*,#3389,.T.);
#4672=ORIENTED_EDGE('',*,*,#3386,.T.);
#4673=ORIENTED_EDGE('',*,*,#3397,.T.);
#4674=ORIENTED_EDGE('',*,*,#3400,.F.);
#4675=ORIENTED_EDGE('',*,*,#3401,.T.);
#4676=ORIENTED_EDGE('',*,*,#3372,.T.);
#4677=ORIENTED_EDGE('',*,*,#3402,.F.);
#4678=ORIENTED_EDGE('',*,*,#3403,.F.);
#4679=ORIENTED_EDGE('',*,*,#3398,.F.);
#4680=ORIENTED_EDGE('',*,*,#3371,.T.);
#4681=ORIENTED_EDGE('',*,*,#3384,.T.);
#4682=ORIENTED_EDGE('',*,*,#3404,.T.);
#4683=ORIENTED_EDGE('',*,*,#3402,.T.);
#4684=ORIENTED_EDGE('',*,*,#3405,.T.);
#4685=ORIENTED_EDGE('',*,*,#3406,.T.);
#4686=ORIENTED_EDGE('',*,*,#3391,.T.);
#4687=ORIENTED_EDGE('',*,*,#3407,.T.);
#4688=ORIENTED_EDGE('',*,*,#3408,.T.);
#4689=ORIENTED_EDGE('',*,*,#3409,.T.);
#4690=ORIENTED_EDGE('',*,*,#3392,.T.);
#4691=ORIENTED_EDGE('',*,*,#3406,.F.);
#4692=ORIENTED_EDGE('',*,*,#3410,.T.);
#4693=ORIENTED_EDGE('',*,*,#3411,.T.);
#4694=ORIENTED_EDGE('',*,*,#3393,.T.);
#4695=ORIENTED_EDGE('',*,*,#3409,.F.);
#4696=ORIENTED_EDGE('',*,*,#3412,.T.);
#4697=ORIENTED_EDGE('',*,*,#3413,.T.);
#4698=ORIENTED_EDGE('',*,*,#3394,.T.);
#4699=ORIENTED_EDGE('',*,*,#3411,.F.);
#4700=ORIENTED_EDGE('',*,*,#3395,.T.);
#4701=ORIENTED_EDGE('',*,*,#3413,.F.);
#4702=ORIENTED_EDGE('',*,*,#3414,.T.);
#4703=ORIENTED_EDGE('',*,*,#3415,.T.);
#4704=ORIENTED_EDGE('',*,*,#3396,.T.);
#4705=ORIENTED_EDGE('',*,*,#3415,.F.);
#4706=ORIENTED_EDGE('',*,*,#3416,.T.);
#4707=ORIENTED_EDGE('',*,*,#3400,.T.);
#4708=ORIENTED_EDGE('',*,*,#3417,.T.);
#4709=ORIENTED_EDGE('',*,*,#3407,.F.);
#4710=ORIENTED_EDGE('',*,*,#3390,.T.);
#4711=ORIENTED_EDGE('',*,*,#3399,.F.);
#4712=ORIENTED_EDGE('',*,*,#3412,.F.);
#4713=ORIENTED_EDGE('',*,*,#3418,.T.);
#4714=ORIENTED_EDGE('',*,*,#3419,.F.);
#4715=ORIENTED_EDGE('',*,*,#3420,.T.);
#4716=ORIENTED_EDGE('',*,*,#3410,.F.);
#4717=ORIENTED_EDGE('',*,*,#3421,.F.);
#4718=ORIENTED_EDGE('',*,*,#3422,.F.);
#4719=ORIENTED_EDGE('',*,*,#3418,.F.);
#4720=ORIENTED_EDGE('',*,*,#3408,.F.);
#4721=ORIENTED_EDGE('',*,*,#3423,.T.);
#4722=ORIENTED_EDGE('',*,*,#3424,.F.);
#4723=ORIENTED_EDGE('',*,*,#3421,.T.);
#4724=ORIENTED_EDGE('',*,*,#3405,.F.);
#4725=ORIENTED_EDGE('',*,*,#3425,.F.);
#4726=ORIENTED_EDGE('',*,*,#3426,.F.);
#4727=ORIENTED_EDGE('',*,*,#3423,.F.);
#4728=ORIENTED_EDGE('',*,*,#3382,.T.);
#4729=ORIENTED_EDGE('',*,*,#3427,.T.);
#4730=ORIENTED_EDGE('',*,*,#3426,.T.);
#4731=ORIENTED_EDGE('',*,*,#3428,.F.);
#4732=ORIENTED_EDGE('',*,*,#3381,.T.);
#4733=ORIENTED_EDGE('',*,*,#3429,.T.);
#4734=ORIENTED_EDGE('',*,*,#3424,.T.);
#4735=ORIENTED_EDGE('',*,*,#3427,.F.);
#4736=ORIENTED_EDGE('',*,*,#3380,.T.);
#4737=ORIENTED_EDGE('',*,*,#3430,.T.);
#4738=ORIENTED_EDGE('',*,*,#3422,.T.);
#4739=ORIENTED_EDGE('',*,*,#3429,.F.);
#4740=ORIENTED_EDGE('',*,*,#3419,.T.);
#4741=ORIENTED_EDGE('',*,*,#3430,.F.);
#4742=ORIENTED_EDGE('',*,*,#3379,.T.);
#4743=ORIENTED_EDGE('',*,*,#3431,.T.);
#4744=ORIENTED_EDGE('',*,*,#3432,.T.);
#4745=ORIENTED_EDGE('',*,*,#3431,.F.);
#4746=ORIENTED_EDGE('',*,*,#3378,.T.);
#4747=ORIENTED_EDGE('',*,*,#3433,.T.);
#4748=ORIENTED_EDGE('',*,*,#3434,.T.);
#4749=ORIENTED_EDGE('',*,*,#3433,.F.);
#4750=ORIENTED_EDGE('',*,*,#3377,.T.);
#4751=ORIENTED_EDGE('',*,*,#3435,.T.);
#4752=ORIENTED_EDGE('',*,*,#3388,.T.);
#4753=ORIENTED_EDGE('',*,*,#3436,.T.);
#4754=ORIENTED_EDGE('',*,*,#3435,.F.);
#4755=ORIENTED_EDGE('',*,*,#3376,.T.);
#4756=ORIENTED_EDGE('',*,*,#3437,.T.);
#4757=ORIENTED_EDGE('',*,*,#3404,.F.);
#4758=ORIENTED_EDGE('',*,*,#3383,.T.);
#4759=ORIENTED_EDGE('',*,*,#3428,.T.);
#4760=ORIENTED_EDGE('',*,*,#3416,.F.);
#4761=ORIENTED_EDGE('',*,*,#3438,.T.);
#4762=ORIENTED_EDGE('',*,*,#3434,.F.);
#4763=ORIENTED_EDGE('',*,*,#3439,.T.);
#4764=ORIENTED_EDGE('',*,*,#3387,.T.);
#4765=ORIENTED_EDGE('',*,*,#3401,.F.);
#4766=ORIENTED_EDGE('',*,*,#3439,.F.);
#4767=ORIENTED_EDGE('',*,*,#3436,.F.);
#4768=ORIENTED_EDGE('',*,*,#3417,.F.);
#4769=ORIENTED_EDGE('',*,*,#3403,.T.);
#4770=ORIENTED_EDGE('',*,*,#3437,.F.);
#4771=ORIENTED_EDGE('',*,*,#3425,.T.);
#4772=ORIENTED_EDGE('',*,*,#3414,.F.);
#4773=ORIENTED_EDGE('',*,*,#3420,.F.);
#4774=ORIENTED_EDGE('',*,*,#3432,.F.);
#4775=ORIENTED_EDGE('',*,*,#3438,.F.);
#5425=CYLINDRICAL_SURFACE('',#6327,3.);
#5426=CYLINDRICAL_SURFACE('',#6331,3.);
#5427=CYLINDRICAL_SURFACE('',#6335,3.);
#5428=CYLINDRICAL_SURFACE('',#6339,2.);
#5429=CYLINDRICAL_SURFACE('',#6342,2.);
#5430=CYLINDRICAL_SURFACE('',#6344,2.);
#5431=CYLINDRICAL_SURFACE('',#6346,2.);
#5432=CYLINDRICAL_SURFACE('',#6356,1.);
#5433=CYLINDRICAL_SURFACE('',#6358,1.);
#5434=CYLINDRICAL_SURFACE('',#6361,1.);
#5435=CYLINDRICAL_SURFACE('',#6363,1.);
#5436=CYLINDRICAL_SURFACE('',#6366,1.);
#5437=CYLINDRICAL_SURFACE('',#6368,1.);
#5438=CYLINDRICAL_SURFACE('',#6370,1.);
#5439=CYLINDRICAL_SURFACE('',#6372,1.);
#5440=CYLINDRICAL_SURFACE('',#6374,1.);
#5441=CYLINDRICAL_SURFACE('',#6375,1.);
#5442=CYLINDRICAL_SURFACE('',#6380,1.);
#5443=CYLINDRICAL_SURFACE('',#6383,1.);
#5444=CYLINDRICAL_SURFACE('',#6385,1.);
#5445=CYLINDRICAL_SURFACE('',#6387,1.);
#5446=CYLINDRICAL_SURFACE('',#6389,1.);
#5447=CYLINDRICAL_SURFACE('',#6391,1.);
#5448=CYLINDRICAL_SURFACE('',#6393,1.);
#5449=CYLINDRICAL_SURFACE('',#6394,1.);
#5715=ADVANCED_FACE('',(#652),#5425,.F.);
#5716=ADVANCED_FACE('',(#653),#408,.T.);
#5717=ADVANCED_FACE('',(#654),#5426,.F.);
#5718=ADVANCED_FACE('',(#655),#409,.T.);
#5719=ADVANCED_FACE('',(#656),#5427,.F.);
#5720=ADVANCED_FACE('',(#657),#410,.T.);
#5721=ADVANCED_FACE('',(#658),#5428,.T.);
#5722=ADVANCED_FACE('',(#659),#5429,.T.);
#5723=ADVANCED_FACE('',(#660),#5430,.T.);
#5724=ADVANCED_FACE('',(#661),#5431,.T.);
#5725=ADVANCED_FACE('',(#662),#411,.T.);
#5726=ADVANCED_FACE('',(#663),#412,.T.);
#5727=ADVANCED_FACE('',(#664,#305,#306,#307),#413,.T.);
#5728=ADVANCED_FACE('',(#665),#414,.T.);
#5729=ADVANCED_FACE('',(#666),#415,.F.);
#5730=ADVANCED_FACE('',(#667),#5432,.T.);
#5731=ADVANCED_FACE('',(#668),#5433,.T.);
#5732=ADVANCED_FACE('',(#669),#416,.T.);
#5733=ADVANCED_FACE('',(#670),#5434,.T.);
#5734=ADVANCED_FACE('',(#671),#5435,.T.);
#5735=ADVANCED_FACE('',(#672),#5436,.T.);
#5736=ADVANCED_FACE('',(#673),#5437,.T.);
#5737=ADVANCED_FACE('',(#674),#5438,.T.);
#5738=ADVANCED_FACE('',(#675),#5439,.T.);
#5739=ADVANCED_FACE('',(#676),#5440,.T.);
#5740=ADVANCED_FACE('',(#677),#5441,.T.);
#5741=ADVANCED_FACE('',(#678),#417,.T.);
#5742=ADVANCED_FACE('',(#679),#418,.T.);
#5743=ADVANCED_FACE('',(#680),#419,.T.);
#5744=ADVANCED_FACE('',(#681),#420,.T.);
#5745=ADVANCED_FACE('',(#682),#5442,.T.);
#5746=ADVANCED_FACE('',(#683),#5443,.T.);
#5747=ADVANCED_FACE('',(#684),#5444,.T.);
#5748=ADVANCED_FACE('',(#685),#5445,.T.);
#5749=ADVANCED_FACE('',(#686),#5446,.T.);
#5750=ADVANCED_FACE('',(#687),#5447,.T.);
#5751=ADVANCED_FACE('',(#688),#5448,.T.);
#5752=ADVANCED_FACE('',(#689),#5449,.T.);
#5753=ADVANCED_FACE('',(#690),#421,.T.);
#5754=ADVANCED_FACE('',(#691),#422,.T.);
#5755=ADVANCED_FACE('',(#692),#423,.T.);
#5756=ADVANCED_FACE('',(#693),#424,.T.);
#5885=CLOSED_SHELL('',(#5715,#5716,#5717,#5718,#5719,#5720,#5721,#5722,
#5723,#5724,#5725,#5726,#5727,#5728,#5729,#5730,#5731,#5732,#5733,#5734,
#5735,#5736,#5737,#5738,#5739,#5740,#5741,#5742,#5743,#5744,#5745,#5746,
#5747,#5748,#5749,#5750,#5751,#5752,#5753,#5754,#5755,#5756));
#6326=AXIS2_PLACEMENT_3D('',#9349,#7575,#7576);
#6327=AXIS2_PLACEMENT_3D('',#9350,#7577,#7578);
#6328=AXIS2_PLACEMENT_3D('',#9352,#7579,#7580);
#6329=AXIS2_PLACEMENT_3D('',#9355,#7582,#7583);
#6330=AXIS2_PLACEMENT_3D('',#9356,#7584,#7585);
#6331=AXIS2_PLACEMENT_3D('',#9357,#7586,#7587);
#6332=AXIS2_PLACEMENT_3D('',#9359,#7588,#7589);
#6333=AXIS2_PLACEMENT_3D('',#9362,#7591,#7592);
#6334=AXIS2_PLACEMENT_3D('',#9363,#7593,#7594);
#6335=AXIS2_PLACEMENT_3D('',#9364,#7595,#7596);
#6336=AXIS2_PLACEMENT_3D('',#9366,#7597,#7598);
#6337=AXIS2_PLACEMENT_3D('',#9369,#7600,#7601);
#6338=AXIS2_PLACEMENT_3D('',#9370,#7602,#7603);
#6339=AXIS2_PLACEMENT_3D('',#9371,#7604,#7605);
#6340=AXIS2_PLACEMENT_3D('',#9376,#7607,#7608);
#6341=AXIS2_PLACEMENT_3D('',#9379,#7610,#7611);
#6342=AXIS2_PLACEMENT_3D('',#9380,#7612,#7613);
#6343=AXIS2_PLACEMENT_3D('',#9385,#7616,#7617);
#6344=AXIS2_PLACEMENT_3D('',#9386,#7618,#7619);
#6345=AXIS2_PLACEMENT_3D('',#9391,#7622,#7623);
#6346=AXIS2_PLACEMENT_3D('',#9392,#7624,#7625);
#6347=AXIS2_PLACEMENT_3D('',#9395,#7628,#7629);
#6348=AXIS2_PLACEMENT_3D('',#9399,#7631,#7632);
#6349=AXIS2_PLACEMENT_3D('',#9403,#7634,#7635);
#6350=AXIS2_PLACEMENT_3D('',#9405,#7637,#7638);
#6351=AXIS2_PLACEMENT_3D('',#9425,#7649,#7650);
#6352=AXIS2_PLACEMENT_3D('',#9426,#7651,#7652);
#6353=AXIS2_PLACEMENT_3D('',#9430,#7654,#7655);
#6354=AXIS2_PLACEMENT_3D('',#9433,#7657,#7658);
#6355=AXIS2_PLACEMENT_3D('',#9434,#7659,#7660);
#6356=AXIS2_PLACEMENT_3D('',#9452,#7670,#7671);
#6357=AXIS2_PLACEMENT_3D('',#9455,#7673,#7674);
#6358=AXIS2_PLACEMENT_3D('',#9456,#7675,#7676);
#6359=AXIS2_PLACEMENT_3D('',#9458,#7677,#7678);
#6360=AXIS2_PLACEMENT_3D('',#9460,#7680,#7681);
#6361=AXIS2_PLACEMENT_3D('',#9464,#7684,#7685);
#6362=AXIS2_PLACEMENT_3D('',#9465,#7686,#7687);
#6363=AXIS2_PLACEMENT_3D('',#9466,#7688,#7689);
#6364=AXIS2_PLACEMENT_3D('',#9470,#7691,#7692);
#6365=AXIS2_PLACEMENT_3D('',#9471,#7693,#7694);
#6366=AXIS2_PLACEMENT_3D('',#9472,#7695,#7696);
#6367=AXIS2_PLACEMENT_3D('',#9475,#7698,#7699);
#6368=AXIS2_PLACEMENT_3D('',#9476,#7700,#7701);
#6369=AXIS2_PLACEMENT_3D('',#9479,#7703,#7704);
#6370=AXIS2_PLACEMENT_3D('',#9480,#7705,#7706);
#6371=AXIS2_PLACEMENT_3D('',#9483,#7708,#7709);
#6372=AXIS2_PLACEMENT_3D('',#9484,#7710,#7711);
#6373=AXIS2_PLACEMENT_3D('',#9487,#7713,#7714);
#6374=AXIS2_PLACEMENT_3D('',#9488,#7715,#7716);
#6375=AXIS2_PLACEMENT_3D('',#9490,#7718,#7719);
#6376=AXIS2_PLACEMENT_3D('',#9492,#7721,#7722);
#6377=AXIS2_PLACEMENT_3D('',#9498,#7726,#7727);
#6378=AXIS2_PLACEMENT_3D('',#9502,#7730,#7731);
#6379=AXIS2_PLACEMENT_3D('',#9506,#7734,#7735);
#6380=AXIS2_PLACEMENT_3D('',#9510,#7738,#7739);
#6381=AXIS2_PLACEMENT_3D('',#9511,#7740,#7741);
#6382=AXIS2_PLACEMENT_3D('',#9512,#7742,#7743);
#6383=AXIS2_PLACEMENT_3D('',#9513,#7744,#7745);
#6384=AXIS2_PLACEMENT_3D('',#9514,#7746,#7747);
#6385=AXIS2_PLACEMENT_3D('',#9515,#7748,#7749);
#6386=AXIS2_PLACEMENT_3D('',#9516,#7750,#7751);
#6387=AXIS2_PLACEMENT_3D('',#9517,#7752,#7753);
#6388=AXIS2_PLACEMENT_3D('',#9518,#7754,#7755);
#6389=AXIS2_PLACEMENT_3D('',#9519,#7756,#7757);
#6390=AXIS2_PLACEMENT_3D('',#9522,#7759,#7760);
#6391=AXIS2_PLACEMENT_3D('',#9523,#7761,#7762);
#6392=AXIS2_PLACEMENT_3D('',#9526,#7764,#7765);
#6393=AXIS2_PLACEMENT_3D('',#9527,#7766,#7767);
#6394=AXIS2_PLACEMENT_3D('',#9529,#7769,#7770);
#6395=AXIS2_PLACEMENT_3D('',#9531,#7772,#7773);
#6396=AXIS2_PLACEMENT_3D('',#9534,#7776,#7777);
#6397=AXIS2_PLACEMENT_3D('',#9535,#7778,#7779);
#6398=AXIS2_PLACEMENT_3D('',#9536,#7780,#7781);
#7575=DIRECTION('axis',(0.,0.,1.));
#7576=DIRECTION('refdir',(1.,0.,0.));
#7577=DIRECTION('center_axis',(0.,0.,-1.));
#7578=DIRECTION('ref_axis',(-1.,0.,0.));
#7579=DIRECTION('center_axis',(0.,0.,-1.));
#7580=DIRECTION('ref_axis',(-1.,0.,0.));
#7581=DIRECTION('',(0.,0.,-1.));
#7582=DIRECTION('center_axis',(0.,0.,-1.));
#7583=DIRECTION('ref_axis',(-1.,0.,0.));
#7584=DIRECTION('center_axis',(0.,0.,1.));
#7585=DIRECTION('ref_axis',(-1.,0.,0.));
#7586=DIRECTION('center_axis',(0.,0.,-1.));
#7587=DIRECTION('ref_axis',(-1.,0.,0.));
#7588=DIRECTION('center_axis',(0.,0.,-1.));
#7589=DIRECTION('ref_axis',(-1.,0.,0.));
#7590=DIRECTION('',(0.,0.,-1.));
#7591=DIRECTION('center_axis',(0.,0.,-1.));
#7592=DIRECTION('ref_axis',(-1.,0.,0.));
#7593=DIRECTION('center_axis',(0.,0.,1.));
#7594=DIRECTION('ref_axis',(-1.,0.,0.));
#7595=DIRECTION('center_axis',(0.,0.,-1.));
#7596=DIRECTION('ref_axis',(-1.,0.,0.));
#7597=DIRECTION('center_axis',(0.,0.,-1.));
#7598=DIRECTION('ref_axis',(-1.,0.,0.));
#7599=DIRECTION('',(0.,0.,-1.));
#7600=DIRECTION('center_axis',(0.,0.,-1.));
#7601=DIRECTION('ref_axis',(-1.,0.,0.));
#7602=DIRECTION('center_axis',(0.,0.,1.));
#7603=DIRECTION('ref_axis',(-1.,0.,0.));
#7604=DIRECTION('center_axis',(1.,0.,0.));
#7605=DIRECTION('ref_axis',(0.,-0.707106781186557,0.707106781186538));
#7606=DIRECTION('',(-1.,0.,0.));
#7607=DIRECTION('center_axis',(0.707106781186548,-0.707106781186548,0.));
#7608=DIRECTION('ref_axis',(-0.707106781186548,-0.707106781186548,0.));
#7609=DIRECTION('',(1.,0.,0.));
#7610=DIRECTION('center_axis',(-0.707106781186548,-0.707106781186547,-1.5700924586838E-15));
#7611=DIRECTION('ref_axis',(-0.707106781186547,0.707106781186548,1.5700924586838E-15));
#7612=DIRECTION('center_axis',(0.,1.,0.));
#7613=DIRECTION('ref_axis',(-0.707106781186549,0.,0.707106781186546));
#7614=DIRECTION('',(0.,-1.,0.));
#7615=DIRECTION('',(0.,1.,0.));
#7616=DIRECTION('center_axis',(-0.707106781186549,-0.707106781186546,0.));
#7617=DIRECTION('ref_axis',(0.707106781186546,-0.707106781186549,0.));
#7618=DIRECTION('center_axis',(0.,1.,0.));
#7619=DIRECTION('ref_axis',(0.707106781186549,0.,0.707106781186546));
#7620=DIRECTION('',(0.,-1.,0.));
#7621=DIRECTION('',(0.,1.,0.));
#7622=DIRECTION('center_axis',(0.707106781186549,-0.707106781186546,-1.57009245868378E-15));
#7623=DIRECTION('ref_axis',(-0.707106781186546,-0.707106781186549,1.57009245868378E-15));
#7624=DIRECTION('center_axis',(1.,0.,0.));
#7625=DIRECTION('ref_axis',(0.,0.707106781186551,0.707106781186544));
#7626=DIRECTION('',(-1.,0.,0.));
#7627=DIRECTION('',(1.,0.,0.));
#7628=DIRECTION('center_axis',(1.,0.,0.));
#7629=DIRECTION('ref_axis',(0.,0.,-1.));
#7630=DIRECTION('',(0.,0.,-1.));
#7631=DIRECTION('center_axis',(1.,0.,0.));
#7632=DIRECTION('ref_axis',(0.,-0.707106781186554,0.707106781186541));
#7633=DIRECTION('',(0.,-1.,0.));
#7634=DIRECTION('center_axis',(1.,0.,0.));
#7635=DIRECTION('ref_axis',(0.,0.707106781186541,0.707106781186554));
#7636=DIRECTION('',(0.,0.,-1.));
#7637=DIRECTION('center_axis',(0.,-1.,0.));
#7638=DIRECTION('ref_axis',(0.,0.,-1.));
#7639=DIRECTION('',(0.,0.,1.));
#7640=DIRECTION('',(1.,0.,0.));
#7641=DIRECTION('',(0.707106781186548,0.,0.707106781186548));
#7642=DIRECTION('',(0.,0.,1.));
#7643=DIRECTION('',(-0.707106781186548,0.,0.707106781186548));
#7644=DIRECTION('',(-1.,0.,0.));
#7645=DIRECTION('',(-0.707106781186548,0.,-0.707106781186548));
#7646=DIRECTION('',(0.,0.,-1.));
#7647=DIRECTION('',(0.707106781186548,0.,-0.707106781186548));
#7648=DIRECTION('',(1.,0.,0.));
#7649=DIRECTION('center_axis',(0.,0.,1.));
#7650=DIRECTION('ref_axis',(1.,0.,0.));
#7651=DIRECTION('center_axis',(-1.,0.,0.));
#7652=DIRECTION('ref_axis',(0.,0.,1.));
#7653=DIRECTION('',(0.,0.,1.));
#7654=DIRECTION('center_axis',(-1.,0.,0.));
#7655=DIRECTION('ref_axis',(0.,0.707106781186541,0.707106781186554));
#7656=DIRECTION('',(0.,1.,0.));
#7657=DIRECTION('center_axis',(-1.,0.,0.));
#7658=DIRECTION('ref_axis',(0.,-0.707106781186554,0.707106781186541));
#7659=DIRECTION('center_axis',(0.,-1.,0.));
#7660=DIRECTION('ref_axis',(-1.,0.,0.));
#7661=DIRECTION('',(-1.,0.,0.));
#7662=DIRECTION('',(-0.707106781186548,0.,0.707106781186548));
#7663=DIRECTION('',(0.,0.,1.));
#7664=DIRECTION('',(0.707106781186548,0.,0.707106781186548));
#7665=DIRECTION('',(1.,0.,0.));
#7666=DIRECTION('',(0.707106781186548,0.,-0.707106781186548));
#7667=DIRECTION('',(0.,0.,-1.));
#7668=DIRECTION('',(-0.707106781186548,0.,-0.707106781186548));
#7669=DIRECTION('',(-1.,0.,0.));
#7670=DIRECTION('center_axis',(-1.,0.,0.));
#7671=DIRECTION('ref_axis',(0.,0.707106781186541,0.707106781186554));
#7672=DIRECTION('',(1.,0.,0.));
#7673=DIRECTION('center_axis',(-0.923879532511291,0.,0.382683432365079));
#7674=DIRECTION('ref_axis',(0.382683432365079,0.,0.923879532511291));
#7675=DIRECTION('center_axis',(-1.,0.,0.));
#7676=DIRECTION('ref_axis',(0.,0.707106781186541,0.707106781186554));
#7677=DIRECTION('center_axis',(-0.923879532511291,0.,-0.382683432365079));
#7678=DIRECTION('ref_axis',(-0.382683432365079,0.,0.923879532511291));
#7679=DIRECTION('',(1.,0.,0.));
#7680=DIRECTION('center_axis',(0.,0.,1.));
#7681=DIRECTION('ref_axis',(-1.,0.,0.));
#7682=DIRECTION('',(-1.,0.,0.));
#7683=DIRECTION('',(0.,-1.,0.));
#7684=DIRECTION('center_axis',(-1.,0.,0.));
#7685=DIRECTION('ref_axis',(0.,-0.707106781186554,0.707106781186541));
#7686=DIRECTION('center_axis',(-0.923879532511283,0.,0.382683432365099));
#7687=DIRECTION('ref_axis',(0.382683432365099,0.,0.923879532511283));
#7688=DIRECTION('center_axis',(0.,0.,1.));
#7689=DIRECTION('ref_axis',(0.707106781186548,0.707106781186548,0.));
#7690=DIRECTION('',(0.,0.,-1.));
#7691=DIRECTION('center_axis',(0.382683432365099,-8.20569863179165E-15,
0.923879532511283));
#7692=DIRECTION('ref_axis',(0.923879532511283,-1.98103089256172E-14,-0.382683432365098));
#7693=DIRECTION('center_axis',(0.382683432365092,-1.98103089256178E-14,
-0.923879532511286));
#7694=DIRECTION('ref_axis',(-0.923879532511286,4.78263164830271E-14,-0.382683432365092));
#7695=DIRECTION('center_axis',(0.707106781186548,0.,0.707106781186548));
#7696=DIRECTION('ref_axis',(0.499999999999999,0.707106781186545,-0.500000000000005));
#7697=DIRECTION('',(-0.707106781186548,0.,-0.707106781186548));
#7698=DIRECTION('center_axis',(0.923879532511283,0.,0.382683432365099));
#7699=DIRECTION('ref_axis',(0.382683432365099,0.,-0.923879532511283));
#7700=DIRECTION('center_axis',(1.,0.,0.));
#7701=DIRECTION('ref_axis',(0.,0.707106781186548,-0.707106781186548));
#7702=DIRECTION('',(-1.,0.,0.));
#7703=DIRECTION('center_axis',(0.923879532511286,1.69945583101724E-15,-0.382683432365092));
#7704=DIRECTION('ref_axis',(-0.382683432365092,4.10284931589584E-15,-0.923879532511286));
#7705=DIRECTION('center_axis',(0.707106781186548,0.,-0.707106781186548));
#7706=DIRECTION('ref_axis',(-0.5,0.707106781186547,-0.5));
#7707=DIRECTION('',(-0.707106781186548,0.,0.707106781186548));
#7708=DIRECTION('center_axis',(0.382683432365092,0.,-0.923879532511286));
#7709=DIRECTION('ref_axis',(-0.923879532511286,0.,-0.382683432365091));
#7710=DIRECTION('center_axis',(0.,0.,-1.));
#7711=DIRECTION('ref_axis',(-0.707106781186548,0.707106781186548,0.));
#7712=DIRECTION('',(0.,0.,1.));
#7713=DIRECTION('center_axis',(-0.382683432365106,0.,-0.92387953251128));
#7714=DIRECTION('ref_axis',(-0.92387953251128,0.,0.382683432365106));
#7715=DIRECTION('center_axis',(-0.707106781186548,0.,-0.707106781186548));
#7716=DIRECTION('ref_axis',(-0.5,0.707106781186547,0.5));
#7717=DIRECTION('',(0.707106781186548,0.,0.707106781186548));
#7718=DIRECTION('center_axis',(-0.707106781186548,0.,0.707106781186548));
#7719=DIRECTION('ref_axis',(0.5,0.707106781186547,0.5));
#7720=DIRECTION('',(0.707106781186548,0.,-0.707106781186548));
#7721=DIRECTION('center_axis',(-0.707106781186548,0.,-0.707106781186548));
#7722=DIRECTION('ref_axis',(-0.707106781186548,0.,0.707106781186548));
#7723=DIRECTION('',(0.,-1.,0.));
#7724=DIRECTION('',(0.707106781186548,0.,-0.707106781186548));
#7725=DIRECTION('',(0.,1.,0.));
#7726=DIRECTION('center_axis',(0.,0.,-1.));
#7727=DIRECTION('ref_axis',(1.,0.,0.));
#7728=DIRECTION('',(0.,1.,0.));
#7729=DIRECTION('',(1.,0.,0.));
#7730=DIRECTION('center_axis',(0.707106781186548,0.,-0.707106781186548));
#7731=DIRECTION('ref_axis',(-0.707106781186548,0.,-0.707106781186548));
#7732=DIRECTION('',(0.,-1.,0.));
#7733=DIRECTION('',(0.707106781186548,0.,0.707106781186548));
#7734=DIRECTION('center_axis',(1.,0.,0.));
#7735=DIRECTION('ref_axis',(0.,0.,1.));
#7736=DIRECTION('',(0.,1.,0.));
#7737=DIRECTION('',(0.,0.,1.));
#7738=DIRECTION('center_axis',(0.,0.,1.));
#7739=DIRECTION('ref_axis',(0.707106781186548,-0.707106781186548,0.));
#7740=DIRECTION('center_axis',(0.382683432365099,8.20569863179165E-15,0.923879532511283));
#7741=DIRECTION('ref_axis',(0.923879532511283,1.98103089256172E-14,-0.382683432365098));
#7742=DIRECTION('center_axis',(-0.382683432365106,1.64113972635832E-14,
0.92387953251128));
#7743=DIRECTION('ref_axis',(-0.92387953251128,-3.96206178512373E-14,-0.382683432365105));
#7744=DIRECTION('center_axis',(-0.707106781186548,0.,-0.707106781186548));
#7745=DIRECTION('ref_axis',(0.499999999999999,-0.707106781186545,-0.500000000000005));
#7746=DIRECTION('center_axis',(0.923879532511284,0.,0.382683432365097));
#7747=DIRECTION('ref_axis',(-0.382683432365097,0.,0.923879532511284));
#7748=DIRECTION('center_axis',(1.,0.,0.));
#7749=DIRECTION('ref_axis',(0.,-0.707106781186544,-0.707106781186551));
#7750=DIRECTION('center_axis',(0.923879532511287,0.,-0.38268343236509));
#7751=DIRECTION('ref_axis',(-0.38268343236509,0.,-0.923879532511287));
#7752=DIRECTION('center_axis',(-0.707106781186548,0.,0.707106781186548));
#7753=DIRECTION('ref_axis',(-0.5,-0.707106781186547,-0.5));
#7754=DIRECTION('center_axis',(0.382683432365092,0.,-0.923879532511286));
#7755=DIRECTION('ref_axis',(0.923879532511286,0.,0.382683432365091));
#7756=DIRECTION('center_axis',(0.,0.,-1.));
#7757=DIRECTION('ref_axis',(-0.707106781186548,-0.707106781186548,0.));
#7758=DIRECTION('',(0.,0.,-1.));
#7759=DIRECTION('center_axis',(-0.382683432365106,0.,-0.92387953251128));
#7760=DIRECTION('ref_axis',(-0.92387953251128,0.,0.382683432365106));
#7761=DIRECTION('center_axis',(0.707106781186548,0.,0.707106781186548));
#7762=DIRECTION('ref_axis',(-0.5,-0.707106781186547,0.5));
#7763=DIRECTION('',(-0.707106781186548,0.,-0.707106781186548));
#7764=DIRECTION('center_axis',(-0.923879532511283,0.,-0.382683432365099));
#7765=DIRECTION('ref_axis',(0.382683432365099,0.,-0.923879532511283));
#7766=DIRECTION('center_axis',(-1.,0.,0.));
#7767=DIRECTION('ref_axis',(0.,-0.707106781186554,0.707106781186541));
#7768=DIRECTION('',(-1.,0.,0.));
#7769=DIRECTION('center_axis',(0.707106781186548,0.,-0.707106781186548));
#7770=DIRECTION('ref_axis',(0.5,-0.707106781186547,0.5));
#7771=DIRECTION('',(-0.707106781186548,0.,0.707106781186548));
#7772=DIRECTION('center_axis',(-0.707106781186548,0.,0.707106781186548));
#7773=DIRECTION('ref_axis',(0.707106781186548,0.,0.707106781186548));
#7774=DIRECTION('',(0.,-1.,0.));
#7775=DIRECTION('',(0.,1.,0.));
#7776=DIRECTION('center_axis',(0.,0.,1.));
#7777=DIRECTION('ref_axis',(-1.,0.,0.));
#7778=DIRECTION('center_axis',(0.707106781186548,0.,0.707106781186548));
#7779=DIRECTION('ref_axis',(0.707106781186548,0.,-0.707106781186548));
#7780=DIRECTION('center_axis',(-1.,0.,0.));
#7781=DIRECTION('ref_axis',(0.,0.,-1.));
#9349=CARTESIAN_POINT('',(0.,0.,0.));
#9350=CARTESIAN_POINT('Origin',(24.1186927691616,-58.,139.));
#9351=CARTESIAN_POINT('',(27.1186927691616,-58.,139.));
#9352=CARTESIAN_POINT('Origin',(24.1186927691616,-58.,139.));
#9353=CARTESIAN_POINT('',(27.1186927691616,-58.,135.));
#9354=CARTESIAN_POINT('',(27.1186927691616,-58.,139.));
#9355=CARTESIAN_POINT('Origin',(24.1186927691616,-58.,135.));
#9356=CARTESIAN_POINT('Origin',(24.1186927691616,-58.,135.));
#9357=CARTESIAN_POINT('Origin',(0.118692769161641,-58.,139.));
#9358=CARTESIAN_POINT('',(3.11869276916164,-58.,139.));
#9359=CARTESIAN_POINT('Origin',(0.118692769161641,-58.,139.));
#9360=CARTESIAN_POINT('',(3.11869276916164,-58.,135.));
#9361=CARTESIAN_POINT('',(3.11869276916164,-58.,139.));
#9362=CARTESIAN_POINT('Origin',(0.118692769161641,-58.,135.));
#9363=CARTESIAN_POINT('Origin',(0.118692769161641,-58.,135.));
#9364=CARTESIAN_POINT('Origin',(-23.8813072308384,-58.,139.));
#9365=CARTESIAN_POINT('',(-20.8813072308384,-58.,139.));
#9366=CARTESIAN_POINT('Origin',(-23.8813072308384,-58.,139.));
#9367=CARTESIAN_POINT('',(-20.8813072308384,-58.,135.));
#9368=CARTESIAN_POINT('',(-20.8813072308384,-58.,139.));
#9369=CARTESIAN_POINT('Origin',(-23.8813072308384,-58.,135.));
#9370=CARTESIAN_POINT('Origin',(-23.8813072308384,-58.,135.));
#9371=CARTESIAN_POINT('Origin',(-16.125,-64.,137.));
#9372=CARTESIAN_POINT('',(31.25,-64.,139.));
#9373=CARTESIAN_POINT('',(-30.75,-64.,139.));
#9374=CARTESIAN_POINT('',(-16.125,-64.,139.));
#9375=CARTESIAN_POINT('',(-32.75,-66.,137.));
#9376=CARTESIAN_POINT('Origin',(-30.75,-64.,137.));
#9377=CARTESIAN_POINT('',(33.25,-66.,137.));
#9378=CARTESIAN_POINT('',(-16.125,-66.,137.));
#9379=CARTESIAN_POINT('Origin',(31.25,-64.,137.));
#9380=CARTESIAN_POINT('Origin',(-30.75,-66.,137.));
#9381=CARTESIAN_POINT('',(-32.75,-50.,137.));
#9382=CARTESIAN_POINT('',(-32.75,-66.,137.));
#9383=CARTESIAN_POINT('',(-30.75,-52.,139.));
#9384=CARTESIAN_POINT('',(-30.75,-66.,139.));
#9385=CARTESIAN_POINT('Origin',(-30.75,-52.,137.));
#9386=CARTESIAN_POINT('Origin',(31.25,-66.,137.));
#9387=CARTESIAN_POINT('',(31.25,-52.,139.));
#9388=CARTESIAN_POINT('',(31.25,-66.,139.));
#9389=CARTESIAN_POINT('',(33.25,-50.,137.));
#9390=CARTESIAN_POINT('',(33.25,-66.,137.));
#9391=CARTESIAN_POINT('Origin',(31.25,-52.,137.));
#9392=CARTESIAN_POINT('Origin',(-16.125,-52.,137.));
#9393=CARTESIAN_POINT('',(-16.125,-50.,137.));
#9394=CARTESIAN_POINT('',(-16.125,-52.,139.));
#9395=CARTESIAN_POINT('Origin',(33.25,-66.,139.));
#9396=CARTESIAN_POINT('',(33.25,-66.,134.));
#9397=CARTESIAN_POINT('',(33.25,-66.,139.));
#9398=CARTESIAN_POINT('',(33.25,-65.,135.));
#9399=CARTESIAN_POINT('Origin',(33.25,-65.,134.));
#9400=CARTESIAN_POINT('',(33.25,-51.,135.));
#9401=CARTESIAN_POINT('',(33.25,-58.,135.));
#9402=CARTESIAN_POINT('',(33.25,-50.,134.));
#9403=CARTESIAN_POINT('Origin',(33.25,-51.,134.));
#9404=CARTESIAN_POINT('',(33.25,-50.,139.));
#9405=CARTESIAN_POINT('Origin',(0.499999999999998,-66.,85.));
#9406=CARTESIAN_POINT('',(-32.75,-66.,134.));
#9407=CARTESIAN_POINT('',(-32.75,-66.,129.));
#9408=CARTESIAN_POINT('',(-44.5857864376269,-66.,134.));
#9409=CARTESIAN_POINT('',(25.5,-66.,134.));
#9410=CARTESIAN_POINT('',(-49.,-66.,129.585786437627));
#9411=CARTESIAN_POINT('',(-46.6678932188135,-66.,131.917893218813));
#9412=CARTESIAN_POINT('',(-49.,-66.,40.4142135623731));
#9413=CARTESIAN_POINT('',(-49.,-66.,110.));
#9414=CARTESIAN_POINT('',(-44.5857864376269,-66.,36.));
#9415=CARTESIAN_POINT('',(-46.6678932188135,-66.,38.0821067811865));
#9416=CARTESIAN_POINT('',(45.0857864376269,-66.,36.));
#9417=CARTESIAN_POINT('',(-24.5,-66.,36.));
#9418=CARTESIAN_POINT('',(49.5,-66.,40.4142135623731));
#9419=CARTESIAN_POINT('',(47.2928932188134,-66.,38.2071067811866));
#9420=CARTESIAN_POINT('',(49.5,-66.,129.585786437627));
#9421=CARTESIAN_POINT('',(49.5,-66.,60.));
#9422=CARTESIAN_POINT('',(45.0857864376269,-66.,134.));
#9423=CARTESIAN_POINT('',(47.2928932188134,-66.,131.792893218813));
#9424=CARTESIAN_POINT('',(25.5,-66.,134.));
#9425=CARTESIAN_POINT('Origin',(-32.75,-66.,139.));
#9426=CARTESIAN_POINT('Origin',(-32.75,-66.,129.));
#9427=CARTESIAN_POINT('',(-32.75,-50.,134.));
#9428=CARTESIAN_POINT('',(-32.75,-50.,129.));
#9429=CARTESIAN_POINT('',(-32.75,-51.,135.));
#9430=CARTESIAN_POINT('Origin',(-32.75,-51.,134.));
#9431=CARTESIAN_POINT('',(-32.75,-65.,135.));
#9432=CARTESIAN_POINT('',(-32.75,-58.,135.));
#9433=CARTESIAN_POINT('Origin',(-32.75,-65.,134.));
#9434=CARTESIAN_POINT('Origin',(0.499999999999998,-50.,85.));
#9435=CARTESIAN_POINT('',(45.0857864376269,-50.,134.));
#9436=CARTESIAN_POINT('',(25.5,-50.,134.));
#9437=CARTESIAN_POINT('',(49.5,-50.,129.585786437627));
#9438=CARTESIAN_POINT('',(47.2928932188134,-50.,131.792893218813));
#9439=CARTESIAN_POINT('',(49.5,-50.,40.4142135623731));
#9440=CARTESIAN_POINT('',(49.5,-50.,60.));
#9441=CARTESIAN_POINT('',(45.0857864376269,-50.,36.));
#9442=CARTESIAN_POINT('',(47.2928932188134,-50.,38.2071067811866));
#9443=CARTESIAN_POINT('',(-44.5857864376269,-50.,36.));
#9444=CARTESIAN_POINT('',(-24.5,-50.,36.));
#9445=CARTESIAN_POINT('',(-49.,-50.,40.4142135623731));
#9446=CARTESIAN_POINT('',(-46.6678932188135,-50.,38.0821067811865));
#9447=CARTESIAN_POINT('',(-49.,-50.,129.585786437627));
#9448=CARTESIAN_POINT('',(-49.,-50.,110.));
#9449=CARTESIAN_POINT('',(-44.5857864376269,-50.,134.));
#9450=CARTESIAN_POINT('',(-46.6678932188135,-50.,131.917893218813));
#9451=CARTESIAN_POINT('',(25.5,-50.,134.));
#9452=CARTESIAN_POINT('Origin',(25.5,-51.,134.));
#9453=CARTESIAN_POINT('',(45.5,-51.,135.));
#9454=CARTESIAN_POINT('',(25.5,-51.,135.));
#9455=CARTESIAN_POINT('Origin',(45.0857864376269,-51.,134.));
#9456=CARTESIAN_POINT('Origin',(25.5,-51.,134.));
#9457=CARTESIAN_POINT('',(-45.,-51.,135.));
#9458=CARTESIAN_POINT('Origin',(-44.5857864376269,-51.,134.));
#9459=CARTESIAN_POINT('',(25.5,-51.,135.));
#9460=CARTESIAN_POINT('Origin',(50.5,-50.,135.));
#9461=CARTESIAN_POINT('',(45.5,-65.,135.));
#9462=CARTESIAN_POINT('',(25.5,-65.,135.));
#9463=CARTESIAN_POINT('',(45.5,-50.,135.));
#9464=CARTESIAN_POINT('Origin',(25.5,-65.,134.));
#9465=CARTESIAN_POINT('Origin',(45.0857864376269,-65.,134.));
#9466=CARTESIAN_POINT('Origin',(49.5,-51.,60.));
#9467=CARTESIAN_POINT('',(50.5,-51.,130.));
#9468=CARTESIAN_POINT('',(50.5,-51.,40.));
#9469=CARTESIAN_POINT('',(50.5,-51.,60.));
#9470=CARTESIAN_POINT('Origin',(49.5,-51.,40.4142135623731));
#9471=CARTESIAN_POINT('Origin',(49.5,-51.,129.585786437627));
#9472=CARTESIAN_POINT('Origin',(47.2928932188134,-51.,38.2071067811866));
#9473=CARTESIAN_POINT('',(45.5,-51.,35.));
#9474=CARTESIAN_POINT('',(48.,-51.,37.5));
#9475=CARTESIAN_POINT('Origin',(45.0857864376269,-51.,36.));
#9476=CARTESIAN_POINT('Origin',(-24.5,-51.,36.));
#9477=CARTESIAN_POINT('',(-45.,-51.,35.));
#9478=CARTESIAN_POINT('',(-24.5,-51.,35.));
#9479=CARTESIAN_POINT('Origin',(-44.5857864376269,-51.,36.));
#9480=CARTESIAN_POINT('Origin',(-46.6678932188135,-51.,38.0821067811865));
#9481=CARTESIAN_POINT('',(-50.,-51.,40.));
#9482=CARTESIAN_POINT('',(-47.375,-51.,37.375));
#9483=CARTESIAN_POINT('Origin',(-49.,-51.,40.4142135623731));
#9484=CARTESIAN_POINT('Origin',(-49.,-51.,110.));
#9485=CARTESIAN_POINT('',(-50.,-51.,130.));
#9486=CARTESIAN_POINT('',(-50.,-51.,110.));
#9487=CARTESIAN_POINT('Origin',(-49.,-51.,129.585786437627));
#9488=CARTESIAN_POINT('Origin',(-46.6678932188135,-51.,131.917893218813));
#9489=CARTESIAN_POINT('',(-47.375,-51.,132.625));
#9490=CARTESIAN_POINT('Origin',(47.2928932188134,-51.,131.792893218813));
#9491=CARTESIAN_POINT('',(48.,-51.,132.5));
#9492=CARTESIAN_POINT('Origin',(-47.5,-50.,37.5));
#9493=CARTESIAN_POINT('',(-45.,-65.,35.));
#9494=CARTESIAN_POINT('',(-45.,-50.,35.));
#9495=CARTESIAN_POINT('',(-50.,-65.,40.));
#9496=CARTESIAN_POINT('',(-47.375,-65.,37.375));
#9497=CARTESIAN_POINT('',(-50.,-50.,40.));
#9498=CARTESIAN_POINT('Origin',(-49.5,-50.,35.));
#9499=CARTESIAN_POINT('',(45.5,-65.,35.));
#9500=CARTESIAN_POINT('',(45.5,-50.,35.));
#9501=CARTESIAN_POINT('',(-24.5,-65.,35.));
#9502=CARTESIAN_POINT('Origin',(48.,-50.,37.5));
#9503=CARTESIAN_POINT('',(50.5,-65.,40.));
#9504=CARTESIAN_POINT('',(50.5,-50.,40.));
#9505=CARTESIAN_POINT('',(48.,-65.,37.5));
#9506=CARTESIAN_POINT('Origin',(50.5,-50.,35.));
#9507=CARTESIAN_POINT('',(50.5,-65.,130.));
#9508=CARTESIAN_POINT('',(50.5,-50.,130.));
#9509=CARTESIAN_POINT('',(50.5,-65.,60.));
#9510=CARTESIAN_POINT('Origin',(49.5,-65.,60.));
#9511=CARTESIAN_POINT('Origin',(49.5,-65.,40.4142135623731));
#9512=CARTESIAN_POINT('Origin',(49.5,-65.,129.585786437627));
#9513=CARTESIAN_POINT('Origin',(47.2928932188134,-65.,38.2071067811866));
#9514=CARTESIAN_POINT('Origin',(45.0857864376269,-65.,36.));
#9515=CARTESIAN_POINT('Origin',(-24.5,-65.,36.));
#9516=CARTESIAN_POINT('Origin',(-44.5857864376269,-65.,36.));
#9517=CARTESIAN_POINT('Origin',(-46.6678932188135,-65.,38.0821067811865));
#9518=CARTESIAN_POINT('Origin',(-49.,-65.,40.4142135623731));
#9519=CARTESIAN_POINT('Origin',(-49.,-65.,110.));
#9520=CARTESIAN_POINT('',(-50.,-65.,130.));
#9521=CARTESIAN_POINT('',(-50.,-65.,110.));
#9522=CARTESIAN_POINT('Origin',(-49.,-65.,129.585786437627));
#9523=CARTESIAN_POINT('Origin',(-46.6678932188135,-65.,131.917893218813));
#9524=CARTESIAN_POINT('',(-45.,-65.,135.));
#9525=CARTESIAN_POINT('',(-47.375,-65.,132.625));
#9526=CARTESIAN_POINT('Origin',(-44.5857864376269,-65.,134.));
#9527=CARTESIAN_POINT('Origin',(25.5,-65.,134.));
#9528=CARTESIAN_POINT('',(25.5,-65.,135.));
#9529=CARTESIAN_POINT('Origin',(47.2928932188134,-65.,131.792893218813));
#9530=CARTESIAN_POINT('',(48.,-65.,132.5));
#9531=CARTESIAN_POINT('Origin',(-47.5,-50.,132.5));
#9532=CARTESIAN_POINT('',(-50.,-50.,130.));
#9533=CARTESIAN_POINT('',(-45.,-50.,135.));
#9534=CARTESIAN_POINT('Origin',(50.5,-50.,135.));
#9535=CARTESIAN_POINT('Origin',(48.,-50.,132.5));
#9536=CARTESIAN_POINT('Origin',(-50.,-50.,135.));
#10115=UNCERTAINTY_MEASURE_WITH_UNIT(LENGTH_MEASURE(0.01),#10132,
'DISTANCE_ACCURACY_VALUE',
'Maximum model space distance between geometric entities at asserted c
onnectivities');
#10119=UNCERTAINTY_MEASURE_WITH_UNIT(LENGTH_MEASURE(0.01),#10132,
'DISTANCE_ACCURACY_VALUE',
'Maximum model space distance between geometric entities at asserted c
onnectivities');
#10127=(
GEOMETRIC_REPRESENTATION_CONTEXT(3)
GLOBAL_UNCERTAINTY_ASSIGNED_CONTEXT((#10115))
GLOBAL_UNIT_ASSIGNED_CONTEXT((#10132,#10134,#10135))
REPRESENTATION_CONTEXT('','3D')
);
#10131=(
GEOMETRIC_REPRESENTATION_CONTEXT(3)
GLOBAL_UNCERTAINTY_ASSIGNED_CONTEXT((#10119))
GLOBAL_UNIT_ASSIGNED_CONTEXT((#10132,#10134,#10135))
REPRESENTATION_CONTEXT('','3D')
);
#10132=(
LENGTH_UNIT()
NAMED_UNIT(*)
SI_UNIT(.MILLI.,.METRE.)
);
#10134=(
NAMED_UNIT(*)
PLANE_ANGLE_UNIT()
SI_UNIT($,.RADIAN.)
);
#10135=(
NAMED_UNIT(*)
SI_UNIT($,.STERADIAN.)
SOLID_ANGLE_UNIT()
);
#10143=SHAPE_DEFINITION_REPRESENTATION(#10154,#10175);
#10154=PRODUCT_DEFINITION_SHAPE('',$,#10187);
#10175=SHAPE_REPRESENTATION('',(#6326),#10127);
#10179=PRODUCT_DEFINITION_CONTEXT('part definition',#10214,'design');
#10187=PRODUCT_DEFINITION('Front_Block_01','Front_Block_01',#10198,#10179);
#10198=PRODUCT_DEFINITION_FORMATION('',$,#10223);
#10214=APPLICATION_CONTEXT(
'Core Data for Automotive Mechanical Design Process');
#10215=PRODUCT_CONTEXT('part definition',#10214,'mechanical');
#10223=PRODUCT('Front_Block_01','Front_Block_01',$,(#10215));
#10241=COLOUR_RGB('Dark Blue',0.08,0.2,0.34);
#10242=FILL_AREA_STYLE_COLOUR('',#10241);
#10243=FILL_AREA_STYLE('',(#10242));
#10244=SURFACE_STYLE_FILL_AREA(#10243);
#10245=SURFACE_SIDE_STYLE('',(#10244));
#10246=SURFACE_STYLE_USAGE(.BOTH.,#10245);
#10247=PRESENTATION_STYLE_ASSIGNMENT((#10246));
ENDSEC;
END-ISO-10303-21;
